ISO-10303-21;
HEADER;
/* Generated by software containing ST-Developer
 * from STEP Tools, Inc. (www.steptools.com) 
 */

FILE_DESCRIPTION(
/* description */ ('Spur gear reduction stage 2-1 on bearing plates'),
/* implementation_level */ '2;1');

FILE_NAME(
/* name */ 'Cap Screw - M6x25.step',
/* time_stamp */ '2026-10-28T03:22:07-07:00',
/* author */ (''),
/* organization */ (''),
/* preprocessor_version */ 'ST-DEVELOPER v20.2',
/* originating_system */ 'Autodesk Translation Framework v15.17.0.0',
/* authorisation */ '');

FILE_SCHEMA (('AUTOMOTIVE_DESIGN { 1 0 10303 214 3 1 1 }'));
ENDSEC;

DATA;
#10=MECHANICAL_DESIGN_GEOMETRIC_PRESENTATION_REPRESENTATION('',(#959),#53909);
#830=ORIENTED_CLOSED_SHELL('',*,#11285,.F.);
#836=CONICAL_SURFACE('',#12130,0.475,0.785398163397449);
#837=CONICAL_SURFACE('',#12134,0.485,0.785398163397448);
#838=CONICAL_SURFACE('',#12138,0.31,0.463647609000806);
#839=CONICAL_SURFACE('',#12142,0.27,0.785398163397448);
#859=BREP_WITH_VOIDS('Body1',#11284,(#830));
#873=SHAPE_REPRESENTATION_RELATIONSHIP('SRR','None',#54100,#916);
#916=ADVANCED_BREP_SHAPE_REPRESENTATION('',(#859),#53874);
#959=STYLED_ITEM('',(#54404),#859);
#1177=FACE_BOUND('',#2420,.T.);
#1303=PLANE('',#12128);
#1304=PLANE('',#12136);
#1305=PLANE('',#12144);
#1306=PLANE('',#12145);
#1307=PLANE('',#12146);
#1308=PLANE('',#12147);
#1309=PLANE('',#12148);
#1310=PLANE('',#12149);
#1311=PLANE('',#12150);
#1312=PLANE('',#12151);
#1313=PLANE('',#12152);
#1650=FACE_OUTER_BOUND('',#2415,.T.);
#1651=FACE_OUTER_BOUND('',#2416,.T.);
#1652=FACE_OUTER_BOUND('',#2417,.T.);
#1653=FACE_OUTER_BOUND('',#2418,.T.);
#1654=FACE_OUTER_BOUND('',#2419,.T.);
#1655=FACE_OUTER_BOUND('',#2421,.T.);
#1656=FACE_OUTER_BOUND('',#2422,.T.);
#1657=FACE_OUTER_BOUND('',#2423,.T.);
#1658=FACE_OUTER_BOUND('',#2424,.T.);
#1659=FACE_OUTER_BOUND('',#2425,.T.);
#1660=FACE_OUTER_BOUND('',#2426,.T.);
#1661=FACE_OUTER_BOUND('',#2427,.T.);
#1662=FACE_OUTER_BOUND('',#2428,.T.);
#1663=FACE_OUTER_BOUND('',#2429,.T.);
#1664=FACE_OUTER_BOUND('',#2430,.T.);
#1665=FACE_OUTER_BOUND('',#2431,.T.);
#1666=FACE_OUTER_BOUND('',#2432,.T.);
#2415=EDGE_LOOP('',(#7944));
#2416=EDGE_LOOP('',(#7945,#7946,#7947,#7948));
#2417=EDGE_LOOP('',(#7949,#7950,#7951,#7952));
#2418=EDGE_LOOP('',(#7953,#7954,#7955,#7956));
#2419=EDGE_LOOP('',(#7957));
#2420=EDGE_LOOP('',(#7958));
#2421=EDGE_LOOP('',(#7959,#7960,#7961,#7962));
#2422=EDGE_LOOP('',(#7963,#7964,#7965,#7966));
#2423=EDGE_LOOP('',(#7967,#7968,#7969,#7970));
#2424=EDGE_LOOP('',(#7971));
#2425=EDGE_LOOP('',(#7972,#7973,#7974,#7975));
#2426=EDGE_LOOP('',(#7976,#7977,#7978,#7979));
#2427=EDGE_LOOP('',(#7980,#7981,#7982,#7983));
#2428=EDGE_LOOP('',(#7984,#7985,#7986,#7987));
#2429=EDGE_LOOP('',(#7988,#7989,#7990,#7991));
#2430=EDGE_LOOP('',(#7992,#7993,#7994,#7995));
#2431=EDGE_LOOP('',(#7996,#7997,#7998,#7999,#8000,#8001));
#2432=EDGE_LOOP('',(#8002,#8003,#8004,#8005,#8006,#8007));
#3113=LINE('',#16635,#3754);
#3114=LINE('',#16639,#3755);
#3115=LINE('',#16643,#3756);
#3116=LINE('',#16650,#3757);
#3117=LINE('',#16654,#3758);
#3118=LINE('',#16658,#3759);
#3119=LINE('',#16663,#3760);
#3120=LINE('',#16665,#3761);
#3121=LINE('',#16667,#3762);
#3122=LINE('',#16668,#3763);
#3123=LINE('',#16671,#3764);
#3124=LINE('',#16673,#3765);
#3125=LINE('',#16674,#3766);
#3126=LINE('',#16677,#3767);
#3127=LINE('',#16679,#3768);
#3128=LINE('',#16680,#3769);
#3129=LINE('',#16683,#3770);
#3130=LINE('',#16685,#3771);
#3131=LINE('',#16686,#3772);
#3132=LINE('',#16689,#3773);
#3133=LINE('',#16691,#3774);
#3134=LINE('',#16692,#3775);
#3135=LINE('',#16694,#3776);
#3136=LINE('',#16695,#3777);
#3754=VECTOR('',#13770,0.475);
#3755=VECTOR('',#13775,0.5);
#3756=VECTOR('',#13780,0.485);
#3757=VECTOR('',#13789,0.31);
#3758=VECTOR('',#13794,0.3);
#3759=VECTOR('',#13799,0.27);
#3760=VECTOR('',#13804,1.);
#3761=VECTOR('',#13805,1.);
#3762=VECTOR('',#13806,1.);
#3763=VECTOR('',#13807,1.);
#3764=VECTOR('',#13810,1.);
#3765=VECTOR('',#13811,1.);
#3766=VECTOR('',#13812,1.);
#3767=VECTOR('',#13815,1.);
#3768=VECTOR('',#13816,1.);
#3769=VECTOR('',#13817,1.);
#3770=VECTOR('',#13820,1.);
#3771=VECTOR('',#13821,1.);
#3772=VECTOR('',#13822,1.);
#3773=VECTOR('',#13825,1.);
#3774=VECTOR('',#13826,1.);
#3775=VECTOR('',#13827,1.);
#3776=VECTOR('',#13830,1.);
#3777=VECTOR('',#13831,1.);
#4419=CIRCLE('',#12129,0.45);
#4420=CIRCLE('',#12131,0.5);
#4421=CIRCLE('',#12133,0.5);
#4422=CIRCLE('',#12135,0.47);
#4423=CIRCLE('',#12137,0.32);
#4424=CIRCLE('',#12139,0.2942);
#4425=CIRCLE('',#12141,0.2942);
#4426=CIRCLE('',#12143,0.24);
#4980=VERTEX_POINT('',#16630);
#4981=VERTEX_POINT('',#16633);
#4982=VERTEX_POINT('',#16637);
#4983=VERTEX_POINT('',#16641);
#4984=VERTEX_POINT('',#16645);
#4985=VERTEX_POINT('',#16648);
#4986=VERTEX_POINT('',#16652);
#4987=VERTEX_POINT('',#16656);
#4988=VERTEX_POINT('',#16661);
#4989=VERTEX_POINT('',#16662);
#4990=VERTEX_POINT('',#16664);
#4991=VERTEX_POINT('',#16666);
#4992=VERTEX_POINT('',#16670);
#4993=VERTEX_POINT('',#16672);
#4994=VERTEX_POINT('',#16676);
#4995=VERTEX_POINT('',#16678);
#4996=VERTEX_POINT('',#16682);
#4997=VERTEX_POINT('',#16684);
#4998=VERTEX_POINT('',#16688);
#4999=VERTEX_POINT('',#16690);
#6114=EDGE_CURVE('',#4980,#4980,#4419,.T.);
#6115=EDGE_CURVE('',#4981,#4981,#4420,.T.);
#6116=EDGE_CURVE('',#4981,#4980,#3113,.T.);
#6117=EDGE_CURVE('',#4982,#4982,#4421,.T.);
#6118=EDGE_CURVE('',#4982,#4981,#3114,.T.);
#6119=EDGE_CURVE('',#4983,#4983,#4422,.T.);
#6120=EDGE_CURVE('',#4983,#4982,#3115,.T.);
#6121=EDGE_CURVE('',#4984,#4984,#4423,.T.);
#6122=EDGE_CURVE('',#4985,#4985,#4424,.F.);
#6123=EDGE_CURVE('',#4985,#4984,#3116,.T.);
#6124=EDGE_CURVE('',#4986,#4986,#4425,.F.);
#6125=EDGE_CURVE('',#4986,#4985,#3117,.T.);
#6126=EDGE_CURVE('',#4987,#4987,#4426,.T.);
#6127=EDGE_CURVE('',#4987,#4986,#3118,.T.);
#6128=EDGE_CURVE('',#4988,#4989,#3119,.T.);
#6129=EDGE_CURVE('',#4989,#4990,#3120,.T.);
#6130=EDGE_CURVE('',#4990,#4991,#3121,.T.);
#6131=EDGE_CURVE('',#4988,#4991,#3122,.T.);
#6132=EDGE_CURVE('',#4989,#4992,#3123,.T.);
#6133=EDGE_CURVE('',#4992,#4993,#3124,.T.);
#6134=EDGE_CURVE('',#4993,#4990,#3125,.T.);
#6135=EDGE_CURVE('',#4992,#4994,#3126,.T.);
#6136=EDGE_CURVE('',#4994,#4995,#3127,.T.);
#6137=EDGE_CURVE('',#4995,#4993,#3128,.T.);
#6138=EDGE_CURVE('',#4994,#4996,#3129,.T.);
#6139=EDGE_CURVE('',#4996,#4997,#3130,.T.);
#6140=EDGE_CURVE('',#4997,#4995,#3131,.T.);
#6141=EDGE_CURVE('',#4996,#4998,#3132,.T.);
#6142=EDGE_CURVE('',#4998,#4999,#3133,.T.);
#6143=EDGE_CURVE('',#4999,#4997,#3134,.T.);
#6144=EDGE_CURVE('',#4998,#4988,#3135,.T.);
#6145=EDGE_CURVE('',#4991,#4999,#3136,.T.);
#7944=ORIENTED_EDGE('',*,*,#6114,.F.);
#7945=ORIENTED_EDGE('',*,*,#6115,.F.);
#7946=ORIENTED_EDGE('',*,*,#6116,.T.);
#7947=ORIENTED_EDGE('',*,*,#6114,.T.);
#7948=ORIENTED_EDGE('',*,*,#6116,.F.);
#7949=ORIENTED_EDGE('',*,*,#6117,.F.);
#7950=ORIENTED_EDGE('',*,*,#6118,.T.);
#7951=ORIENTED_EDGE('',*,*,#6115,.T.);
#7952=ORIENTED_EDGE('',*,*,#6118,.F.);
#7953=ORIENTED_EDGE('',*,*,#6119,.F.);
#7954=ORIENTED_EDGE('',*,*,#6120,.T.);
#7955=ORIENTED_EDGE('',*,*,#6117,.T.);
#7956=ORIENTED_EDGE('',*,*,#6120,.F.);
#7957=ORIENTED_EDGE('',*,*,#6119,.T.);
#7958=ORIENTED_EDGE('',*,*,#6121,.F.);
#7959=ORIENTED_EDGE('',*,*,#6122,.F.);
#7960=ORIENTED_EDGE('',*,*,#6123,.T.);
#7961=ORIENTED_EDGE('',*,*,#6121,.T.);
#7962=ORIENTED_EDGE('',*,*,#6123,.F.);
#7963=ORIENTED_EDGE('',*,*,#6124,.F.);
#7964=ORIENTED_EDGE('',*,*,#6125,.T.);
#7965=ORIENTED_EDGE('',*,*,#6122,.T.);
#7966=ORIENTED_EDGE('',*,*,#6125,.F.);
#7967=ORIENTED_EDGE('',*,*,#6126,.F.);
#7968=ORIENTED_EDGE('',*,*,#6127,.T.);
#7969=ORIENTED_EDGE('',*,*,#6124,.T.);
#7970=ORIENTED_EDGE('',*,*,#6127,.F.);
#7971=ORIENTED_EDGE('',*,*,#6126,.T.);
#7972=ORIENTED_EDGE('',*,*,#6128,.T.);
#7973=ORIENTED_EDGE('',*,*,#6129,.T.);
#7974=ORIENTED_EDGE('',*,*,#6130,.T.);
#7975=ORIENTED_EDGE('',*,*,#6131,.F.);
#7976=ORIENTED_EDGE('',*,*,#6132,.T.);
#7977=ORIENTED_EDGE('',*,*,#6133,.T.);
#7978=ORIENTED_EDGE('',*,*,#6134,.T.);
#7979=ORIENTED_EDGE('',*,*,#6129,.F.);
#7980=ORIENTED_EDGE('',*,*,#6135,.T.);
#7981=ORIENTED_EDGE('',*,*,#6136,.T.);
#7982=ORIENTED_EDGE('',*,*,#6137,.T.);
#7983=ORIENTED_EDGE('',*,*,#6133,.F.);
#7984=ORIENTED_EDGE('',*,*,#6138,.T.);
#7985=ORIENTED_EDGE('',*,*,#6139,.T.);
#7986=ORIENTED_EDGE('',*,*,#6140,.T.);
#7987=ORIENTED_EDGE('',*,*,#6136,.F.);
#7988=ORIENTED_EDGE('',*,*,#6141,.T.);
#7989=ORIENTED_EDGE('',*,*,#6142,.T.);
#7990=ORIENTED_EDGE('',*,*,#6143,.T.);
#7991=ORIENTED_EDGE('',*,*,#6139,.F.);
#7992=ORIENTED_EDGE('',*,*,#6144,.T.);
#7993=ORIENTED_EDGE('',*,*,#6131,.T.);
#7994=ORIENTED_EDGE('',*,*,#6145,.T.);
#7995=ORIENTED_EDGE('',*,*,#6142,.F.);
#7996=ORIENTED_EDGE('',*,*,#6144,.F.);
#7997=ORIENTED_EDGE('',*,*,#6141,.F.);
#7998=ORIENTED_EDGE('',*,*,#6138,.F.);
#7999=ORIENTED_EDGE('',*,*,#6135,.F.);
#8000=ORIENTED_EDGE('',*,*,#6132,.F.);
#8001=ORIENTED_EDGE('',*,*,#6128,.F.);
#8002=ORIENTED_EDGE('',*,*,#6145,.F.);
#8003=ORIENTED_EDGE('',*,*,#6130,.F.);
#8004=ORIENTED_EDGE('',*,*,#6134,.F.);
#8005=ORIENTED_EDGE('',*,*,#6137,.F.);
#8006=ORIENTED_EDGE('',*,*,#6140,.F.);
#8007=ORIENTED_EDGE('',*,*,#6143,.F.);
#10498=CYLINDRICAL_SURFACE('',#12132,0.5);
#10499=CYLINDRICAL_SURFACE('',#12140,0.2942);
#10770=ADVANCED_FACE('',(#1650),#1303,.T.);
#10771=ADVANCED_FACE('',(#1651),#836,.T.);
#10772=ADVANCED_FACE('',(#1652),#10498,.T.);
#10773=ADVANCED_FACE('',(#1653),#837,.T.);
#10774=ADVANCED_FACE('',(#1654,#1177),#1304,.T.);
#10775=ADVANCED_FACE('',(#1655),#838,.T.);
#10776=ADVANCED_FACE('',(#1656),#10499,.T.);
#10777=ADVANCED_FACE('',(#1657),#839,.T.);
#10778=ADVANCED_FACE('',(#1658),#1305,.T.);
#10779=ADVANCED_FACE('',(#1659),#1306,.F.);
#10780=ADVANCED_FACE('',(#1660),#1307,.F.);
#10781=ADVANCED_FACE('',(#1661),#1308,.F.);
#10782=ADVANCED_FACE('',(#1662),#1309,.F.);
#10783=ADVANCED_FACE('',(#1663),#1310,.F.);
#10784=ADVANCED_FACE('',(#1664),#1311,.F.);
#10785=ADVANCED_FACE('',(#1665),#1312,.F.);
#10786=ADVANCED_FACE('',(#1666),#1313,.F.);
#11284=CLOSED_SHELL('',(#10770,#10771,#10772,#10773,#10774,#10775,#10776,
#10777,#10778));
#11285=CLOSED_SHELL('',(#10779,#10780,#10781,#10782,#10783,#10784,#10785,
#10786));
#12127=AXIS2_PLACEMENT_3D('',#16628,#13760,#13761);
#12128=AXIS2_PLACEMENT_3D('',#16629,#13762,#13763);
#12129=AXIS2_PLACEMENT_3D('',#16631,#13764,#13765);
#12130=AXIS2_PLACEMENT_3D('',#16632,#13766,#13767);
#12131=AXIS2_PLACEMENT_3D('',#16634,#13768,#13769);
#12132=AXIS2_PLACEMENT_3D('',#16636,#13771,#13772);
#12133=AXIS2_PLACEMENT_3D('',#16638,#13773,#13774);
#12134=AXIS2_PLACEMENT_3D('',#16640,#13776,#13777);
#12135=AXIS2_PLACEMENT_3D('',#16642,#13778,#13779);
#12136=AXIS2_PLACEMENT_3D('',#16644,#13781,#13782);
#12137=AXIS2_PLACEMENT_3D('',#16646,#13783,#13784);
#12138=AXIS2_PLACEMENT_3D('',#16647,#13785,#13786);
#12139=AXIS2_PLACEMENT_3D('',#16649,#13787,#13788);
#12140=AXIS2_PLACEMENT_3D('',#16651,#13790,#13791);
#12141=AXIS2_PLACEMENT_3D('',#16653,#13792,#13793);
#12142=AXIS2_PLACEMENT_3D('',#16655,#13795,#13796);
#12143=AXIS2_PLACEMENT_3D('',#16657,#13797,#13798);
#12144=AXIS2_PLACEMENT_3D('',#16659,#13800,#13801);
#12145=AXIS2_PLACEMENT_3D('',#16660,#13802,#13803);
#12146=AXIS2_PLACEMENT_3D('',#16669,#13808,#13809);
#12147=AXIS2_PLACEMENT_3D('',#16675,#13813,#13814);
#12148=AXIS2_PLACEMENT_3D('',#16681,#13818,#13819);
#12149=AXIS2_PLACEMENT_3D('',#16687,#13823,#13824);
#12150=AXIS2_PLACEMENT_3D('',#16693,#13828,#13829);
#12151=AXIS2_PLACEMENT_3D('',#16696,#13832,#13833);
#12152=AXIS2_PLACEMENT_3D('',#16697,#13834,#13835);
#13760=DIRECTION('axis',(0.,0.,1.));
#13761=DIRECTION('refdir',(1.,0.,0.));
#13762=DIRECTION('center_axis',(0.,1.,0.));
#13763=DIRECTION('ref_axis',(0.,0.,1.));
#13764=DIRECTION('center_axis',(0.,-1.,0.));
#13765=DIRECTION('ref_axis',(1.,0.,0.));
#13766=DIRECTION('center_axis',(0.,-1.,0.));
#13767=DIRECTION('ref_axis',(1.,0.,0.));
#13768=DIRECTION('center_axis',(0.,-1.,0.));
#13769=DIRECTION('ref_axis',(1.,0.,0.));
#13770=DIRECTION('',(0.707106781186548,0.707106781186547,8.65956056235494E-17));
#13771=DIRECTION('center_axis',(0.,-1.,0.));
#13772=DIRECTION('ref_axis',(1.,0.,0.));
#13773=DIRECTION('center_axis',(0.,-1.,0.));
#13774=DIRECTION('ref_axis',(1.,0.,0.));
#13775=DIRECTION('',(0.,1.,0.));
#13776=DIRECTION('center_axis',(0.,1.,0.));
#13777=DIRECTION('ref_axis',(1.,0.,0.));
#13778=DIRECTION('center_axis',(0.,-1.,0.));
#13779=DIRECTION('ref_axis',(1.,0.,0.));
#13780=DIRECTION('',(-0.707106781186547,0.707106781186548,-8.65956056235493E-17));
#13781=DIRECTION('center_axis',(0.,-1.,0.));
#13782=DIRECTION('ref_axis',(0.,0.,-1.));
#13783=DIRECTION('center_axis',(0.,-1.,0.));
#13784=DIRECTION('ref_axis',(1.,0.,0.));
#13785=DIRECTION('center_axis',(0.,1.,0.));
#13786=DIRECTION('ref_axis',(1.,0.,0.));
#13787=DIRECTION('center_axis',(0.,1.,0.));
#13788=DIRECTION('ref_axis',(1.,0.,0.));
#13789=DIRECTION('',(-0.447213595499958,0.894427190999916,-5.47678698264203E-17));
#13790=DIRECTION('center_axis',(0.,-1.,0.));
#13791=DIRECTION('ref_axis',(1.,0.,0.));
#13792=DIRECTION('center_axis',(0.,1.,0.));
#13793=DIRECTION('ref_axis',(1.,0.,0.));
#13794=DIRECTION('',(0.,1.,0.));
#13795=DIRECTION('center_axis',(0.,1.,0.));
#13796=DIRECTION('ref_axis',(1.,0.,0.));
#13797=DIRECTION('center_axis',(0.,-1.,0.));
#13798=DIRECTION('ref_axis',(1.,0.,0.));
#13799=DIRECTION('',(-0.707106781186547,0.707106781186548,-8.65956056235493E-17));
#13800=DIRECTION('center_axis',(0.,-1.,0.));
#13801=DIRECTION('ref_axis',(0.,0.,-1.));
#13802=DIRECTION('center_axis',(0.866025403784439,0.,-0.5));
#13803=DIRECTION('ref_axis',(0.5,0.,0.866025403784439));
#13804=DIRECTION('',(-0.5,0.,-0.866025403784439));
#13805=DIRECTION('',(0.,-1.,0.));
#13806=DIRECTION('',(0.5,0.,0.866025403784439));
#13807=DIRECTION('',(0.,-1.,0.));
#13808=DIRECTION('center_axis',(1.92296268638356E-16,0.,-1.));
#13809=DIRECTION('ref_axis',(1.,0.,1.92296268638356E-16));
#13810=DIRECTION('',(-1.,0.,-1.92296268638356E-16));
#13811=DIRECTION('',(0.,-1.,0.));
#13812=DIRECTION('',(1.,0.,1.92296268638356E-16));
#13813=DIRECTION('center_axis',(-0.866025403784439,0.,-0.5));
#13814=DIRECTION('ref_axis',(0.5,0.,-0.866025403784439));
#13815=DIRECTION('',(-0.5,0.,0.866025403784438));
#13816=DIRECTION('',(0.,-1.,0.));
#13817=DIRECTION('',(0.5,0.,-0.866025403784438));
#13818=DIRECTION('center_axis',(-0.866025403784439,0.,0.5));
#13819=DIRECTION('ref_axis',(-0.5,0.,-0.866025403784439));
#13820=DIRECTION('',(0.5,0.,0.866025403784439));
#13821=DIRECTION('',(0.,-1.,0.));
#13822=DIRECTION('',(-0.5,0.,-0.866025403784439));
#13823=DIRECTION('center_axis',(-1.92296268638356E-16,0.,1.));
#13824=DIRECTION('ref_axis',(-1.,0.,-1.92296268638356E-16));
#13825=DIRECTION('',(1.,0.,1.92296268638356E-16));
#13826=DIRECTION('',(0.,-1.,0.));
#13827=DIRECTION('',(-1.,0.,-1.92296268638356E-16));
#13828=DIRECTION('center_axis',(0.866025403784439,0.,0.5));
#13829=DIRECTION('ref_axis',(-0.5,0.,0.866025403784439));
#13830=DIRECTION('',(0.5,0.,-0.866025403784439));
#13831=DIRECTION('',(-0.5,0.,0.866025403784439));
#13832=DIRECTION('center_axis',(0.,1.,0.));
#13833=DIRECTION('ref_axis',(1.,0.,0.));
#13834=DIRECTION('center_axis',(0.,-1.,0.));
#13835=DIRECTION('ref_axis',(0.,0.,-1.));
#16628=CARTESIAN_POINT('',(0.,0.,0.));
#16629=CARTESIAN_POINT('Origin',(0.45,0.6,0.));
#16630=CARTESIAN_POINT('',(-0.45,0.6,-5.51091059616309E-17));
#16631=CARTESIAN_POINT('Origin',(0.,0.6,0.));
#16632=CARTESIAN_POINT('Origin',(0.,0.575,0.));
#16633=CARTESIAN_POINT('',(-0.5,0.55,-6.12323399573677E-17));
#16634=CARTESIAN_POINT('Origin',(0.,0.55,0.));
#16635=CARTESIAN_POINT('',(-0.475,0.575,-5.81707229594993E-17));
#16636=CARTESIAN_POINT('Origin',(0.,0.29,0.));
#16637=CARTESIAN_POINT('',(-0.5,0.0299999999999998,-6.12323399573677E-17));
#16638=CARTESIAN_POINT('Origin',(0.,0.0299999999999998,0.));
#16639=CARTESIAN_POINT('',(-0.5,0.29,-6.12323399573677E-17));
#16640=CARTESIAN_POINT('Origin',(0.,0.0150000000000001,0.));
#16641=CARTESIAN_POINT('',(-0.47,7.11236625150491E-17,-5.75583995599256E-17));
#16642=CARTESIAN_POINT('Origin',(0.,0.,0.));
#16643=CARTESIAN_POINT('',(-0.485,0.0150000000000001,-5.93953697586466E-17));
#16644=CARTESIAN_POINT('Origin',(0.32,0.,0.));
#16645=CARTESIAN_POINT('',(-0.32,-6.93889390390723E-18,-3.91886975727153E-17));
#16646=CARTESIAN_POINT('Origin',(0.,0.,0.));
#16647=CARTESIAN_POINT('Origin',(0.,-0.02,0.));
#16648=CARTESIAN_POINT('',(-0.2942,-0.0515999999999999,3.60291088309151E-17));
#16649=CARTESIAN_POINT('Origin',(0.,-0.0515999999999999,0.));
#16650=CARTESIAN_POINT('',(-0.31,-0.02,-3.7964050773568E-17));
#16651=CARTESIAN_POINT('Origin',(0.,-1.24,0.));
#16652=CARTESIAN_POINT('',(-0.2942,-2.4458,3.60291088309151E-17));
#16653=CARTESIAN_POINT('Origin',(0.,-2.4458,0.));
#16654=CARTESIAN_POINT('',(-0.2942,-1.24,-3.60291088309151E-17));
#16655=CARTESIAN_POINT('Origin',(0.,-2.47,0.));
#16656=CARTESIAN_POINT('',(-0.24,-2.5,-2.93915231795365E-17));
#16657=CARTESIAN_POINT('Origin',(0.,-2.5,0.));
#16658=CARTESIAN_POINT('',(-0.27,-2.47,-3.30654635769785E-17));
#16659=CARTESIAN_POINT('Origin',(0.,-2.5,0.));
#16660=CARTESIAN_POINT('Origin',(0.144337567297406,-0.6,-0.25));
#16661=CARTESIAN_POINT('',(0.288675134594813,-0.6,0.));
#16662=CARTESIAN_POINT('',(0.144337567297406,-0.6,-0.25));
#16663=CARTESIAN_POINT('',(0.288675134594813,-0.6,0.));
#16664=CARTESIAN_POINT('',(0.144337567297406,-0.96,-0.25));
#16665=CARTESIAN_POINT('',(0.144337567297406,-0.6,-0.25));
#16666=CARTESIAN_POINT('',(0.288675134594813,-0.96,0.));
#16667=CARTESIAN_POINT('',(0.288675134594813,-0.96,0.));
#16668=CARTESIAN_POINT('',(0.288675134594813,-0.6,0.));
#16669=CARTESIAN_POINT('Origin',(-0.144337567297406,-0.6,-0.25));
#16670=CARTESIAN_POINT('',(-0.144337567297406,-0.6,-0.25));
#16671=CARTESIAN_POINT('',(0.144337567297406,-0.6,-0.25));
#16672=CARTESIAN_POINT('',(-0.144337567297406,-0.96,-0.25));
#16673=CARTESIAN_POINT('',(-0.144337567297406,-0.6,-0.25));
#16674=CARTESIAN_POINT('',(0.144337567297406,-0.96,-0.25));
#16675=CARTESIAN_POINT('Origin',(-0.288675134594813,-0.6,-8.32667268468867E-17));
#16676=CARTESIAN_POINT('',(-0.288675134594813,-0.6,-3.53525079574969E-17));
#16677=CARTESIAN_POINT('',(-0.144337567297406,-0.6,-0.25));
#16678=CARTESIAN_POINT('',(-0.288675134594813,-0.96,-5.55111512312578E-17));
#16679=CARTESIAN_POINT('',(-0.288675134594813,-0.6,-3.53525079574969E-17));
#16680=CARTESIAN_POINT('',(-0.144337567297406,-0.96,-0.25));
#16681=CARTESIAN_POINT('Origin',(-0.144337567297407,-0.6,0.25));
#16682=CARTESIAN_POINT('',(-0.144337567297407,-0.6,0.25));
#16683=CARTESIAN_POINT('',(-0.288675134594813,-0.6,-3.53525079574969E-17));
#16684=CARTESIAN_POINT('',(-0.144337567297407,-0.96,0.25));
#16685=CARTESIAN_POINT('',(-0.144337567297407,-0.6,0.25));
#16686=CARTESIAN_POINT('',(-0.288675134594813,-0.96,-3.53525079574969E-17));
#16687=CARTESIAN_POINT('Origin',(0.144337567297406,-0.6,0.25));
#16688=CARTESIAN_POINT('',(0.144337567297406,-0.6,0.25));
#16689=CARTESIAN_POINT('',(-0.144337567297407,-0.6,0.25));
#16690=CARTESIAN_POINT('',(0.144337567297406,-0.96,0.25));
#16691=CARTESIAN_POINT('',(0.144337567297406,-0.6,0.25));
#16692=CARTESIAN_POINT('',(-0.144337567297407,-0.96,0.25));
#16693=CARTESIAN_POINT('Origin',(0.288675134594813,-0.6,0.));
#16694=CARTESIAN_POINT('',(0.144337567297406,-0.6,0.25));
#16695=CARTESIAN_POINT('',(0.144337567297406,-0.96,0.25));
#16696=CARTESIAN_POINT('Origin',(0.,-0.6,0.));
#16697=CARTESIAN_POINT('Origin',(0.,-0.96,0.));
#53824=UNCERTAINTY_MEASURE_WITH_UNIT(LENGTH_MEASURE(0.001),#53910,
'DISTANCE_ACCURACY_VALUE',
'Maximum model space distance between geometric entities at asserted c
onnectivities');
#53859=UNCERTAINTY_MEASURE_WITH_UNIT(LENGTH_MEASURE(0.001),#53910,
'DISTANCE_ACCURACY_VALUE',
'Maximum model space distance between geometric entities at asserted c
onnectivities');
#53874=(
GEOMETRIC_REPRESENTATION_CONTEXT(3)
GLOBAL_UNCERTAINTY_ASSIGNED_CONTEXT((#53824))
GLOBAL_UNIT_ASSIGNED_CONTEXT((#53910,#53912,#53913))
REPRESENTATION_CONTEXT('','3D')
);
#53909=(
GEOMETRIC_REPRESENTATION_CONTEXT(3)
GLOBAL_UNCERTAINTY_ASSIGNED_CONTEXT((#53859))
GLOBAL_UNIT_ASSIGNED_CONTEXT((#53910,#53912,#53913))
REPRESENTATION_CONTEXT('','3D')
);
#53910=(
LENGTH_UNIT()
NAMED_UNIT(*)
SI_UNIT(.CENTI.,.METRE.)
);
#53912=(
NAMED_UNIT(*)
PLANE_ANGLE_UNIT()
SI_UNIT($,.RADIAN.)
);
#53913=(
NAMED_UNIT(*)
SI_UNIT($,.STERADIAN.)
SOLID_ANGLE_UNIT()
);
#53928=SHAPE_DEFINITION_REPRESENTATION(#53977,#54100);
#53977=PRODUCT_DEFINITION_SHAPE('',$,#54150);
#54100=SHAPE_REPRESENTATION('',(#12127),#53874);
#54135=PRODUCT_DEFINITION_CONTEXT('part definition',#54284,'design');
#54150=PRODUCT_DEFINITION('Cap Screw - M6x25','Cap Screw - M6x25',#54199,
#54135);
#54199=PRODUCT_DEFINITION_FORMATION('',$,#54300);
#54284=APPLICATION_CONTEXT(
'Core Data for Automotive Mechanical Design Process');
#54285=PRODUCT_CONTEXT('part definition',#54284,'mechanical');
#54300=PRODUCT('Cap Screw - M6x25','Cap Screw - M6x25',
'Cap Screw - M6x25',(#54285));
#54398=COLOUR_RGB('Black',0.12,0.14,0.17);
#54399=FILL_AREA_STYLE_COLOUR('',#54398);
#54400=FILL_AREA_STYLE('',(#54399));
#54401=SURFACE_STYLE_FILL_AREA(#54400);
#54402=SURFACE_SIDE_STYLE('',(#54401));
#54403=SURFACE_STYLE_USAGE(.BOTH.,#54402);
#54404=PRESENTATION_STYLE_ASSIGNMENT((#54403));
ENDSEC;
END-ISO-10303-21;
